ISO-10303-21;
HEADER;
FILE_DESCRIPTION (('STEP AP214'),
    '1' );
FILE_NAME ('Part5.step',
    '2026-11-01T05:08:46',
    ( '' ),
    ( '' ),
    'SwSTEP 2.0',
    'SolidWorks 2024',
    '' );
FILE_SCHEMA (( 'AUTOMOTIVE_DESIGN' ));
ENDSEC;

DATA;
#11=VERTEX_POINT ( 'NONE', #11668 ) ;
#38=FACE_OUTER_BOUND ( 'NONE', #10293, .T. ) ;
#66=EDGE_CURVE ( 'NONE', #15272, #6025, #13499, .T. ) ;
#70=VECTOR ( 'NONE', #318, 1000.000000000000000 ) ;
#74=EDGE_LOOP ( 'NONE', ( #10191, #4537, #11740, #10605, #6222, #2610, #6694, #4474, #3337 ) ) ;
#84=VECTOR ( 'NONE', #15689, 1000.000000000000000 ) ;
#91=FACE_OUTER_BOUND ( 'NONE', #74, .T. ) ;
#115=ORIENTED_EDGE ( 'NONE', *, *, #13843, .T. ) ;
#126=SURFACE_SIDE_STYLE ('',( #8186 ) ) ;
#137=ORIENTED_EDGE ( 'NONE', *, *, #15607, .T. ) ;
#138=FACE_OUTER_BOUND ( 'NONE', #14559, .T. ) ;
#228=EDGE_LOOP ( 'NONE', ( #821, #15610, #9726, #13446 ) ) ;
#233=DIRECTION ( 'NONE',  ( 1.000000000000000000, -0.000000000000000000, 0.000000000000000000 ) ) ;
#278=VECTOR ( 'NONE', #3201, 1000.000000000000000 ) ;
#310=CARTESIAN_POINT ( 'NONE',  ( 0.000000000000000000, 363.9544815475646260, -322.6258333628447872 ) ) ;
#318=DIRECTION ( 'NONE',  ( 0.000000000000000000, -1.000000000000000000, 0.000000000000000000 ) ) ;
#351=DIRECTION ( 'NONE',  ( 0.000000000000000000, 0.000000000000000000, 1.000000000000000000 ) ) ;
#391=( LENGTH_UNIT ( ) NAMED_UNIT ( * ) SI_UNIT ( .MILLI., .METRE. ) );
#498=EDGE_CURVE ( 'NONE', #5425, #7059, #16112, .T. ) ;
#506=EDGE_CURVE ( 'NONE', #7981, #15905, #4356, .T. ) ;
#536=SHAPE_DEFINITION_REPRESENTATION ( #12591, #584 ) ;
#584=SHAPE_REPRESENTATION ( 'Part5', ( #1488 ), #4776 ) ;
#607=ORIENTED_EDGE ( 'NONE', *, *, #12460, .T. ) ;
#609=DIRECTION ( 'NONE',  ( -1.000000000000000000, -0.000000000000000000, -0.000000000000000000 ) ) ;
#623=AXIS2_PLACEMENT_3D ( 'NONE', #9579, #7932, #13279 ) ;
#643=AXIS2_PLACEMENT_3D ( 'NONE', #5961, #10088, #16359 ) ;
#682=ORIENTED_EDGE ( 'NONE', *, *, #11656, .F. ) ;
#724=ORIENTED_EDGE ( 'NONE', *, *, #10666, .F. ) ;
#785=VERTEX_POINT ( 'NONE', #3897 ) ;
#790=PRODUCT_CONTEXT ( 'NONE', #4781, 'mechanical' ) ;
#821=ORIENTED_EDGE ( 'NONE', *, *, #14805, .T. ) ;
#901=FACE_OUTER_BOUND ( 'NONE', #228, .T. ) ;
#911=DIRECTION ( 'NONE',  ( 1.000000000000000000, 0.000000000000000000, 0.000000000000000000 ) ) ;
#1068=FACE_OUTER_BOUND ( 'NONE', #12225, .T. ) ;
#1218=PRODUCT_DEFINITION_FORMATION_WITH_SPECIFIED_SOURCE ( 'ANY', '', #9625, .NOT_KNOWN. ) ;
#1235=LINE ( 'NONE', #14372, #6109 ) ;
#1245=AXIS2_PLACEMENT_3D ( 'NONE', #2717, #2979, #14407 ) ;
#1262=EDGE_LOOP ( 'NONE', ( #3431, #9130, #16351, #16557, #16838, #8786, #9972, #3959, #8524 ) ) ;
#1279=CIRCLE ( 'NONE', #12264, 10.00000000000061995 ) ;
#1296=LINE ( 'NONE', #5147, #15553 ) ;
#1301=EDGE_CURVE ( 'NONE', #4071, #13919, #1705, .T. ) ;
#1305=EDGE_LOOP ( 'NONE', ( #13296, #8825, #115, #607 ) ) ;
#1363=DIRECTION ( 'NONE',  ( 0.000000000000000000, 0.6366988521258363232, -0.7711125544961918710 ) ) ;
#1405=CIRCLE ( 'NONE', #5517, 30.00000000000002842 ) ;
#1419=LINE ( 'NONE', #8024, #5535 ) ;
#1420=EDGE_CURVE ( 'NONE', #785, #15912, #1419, .T. ) ;
#1465=FACE_OUTER_BOUND ( 'NONE', #7870, .T. ) ;
#1488=AXIS2_PLACEMENT_3D ( 'NONE', #3280, #8693, #15217 ) ;
#1501=VERTEX_POINT ( 'NONE', #13024 ) ;
#1510=CARTESIAN_POINT ( 'NONE',  ( 10.00000000000000000, 374.2147300931088694, -220.2054496871573974 ) ) ;
#1563=ORIENTED_EDGE ( 'NONE', *, *, #4283, .T. ) ;
#1593=PLANE ( 'NONE',  #623 ) ;
#1601=CARTESIAN_POINT ( 'NONE',  ( 10.00000000000000000, 34.88079231221936283, 28.80067286797032722 ) ) ;
#1635=CARTESIAN_POINT ( 'NONE',  ( 10.00000000000000000, 435.2933666400819561, -550.3792044179907634 ) ) ;
#1662=CARTESIAN_POINT ( 'NONE',  ( 0.000000000000000000, 435.2933666400819561, -525.1288175801793159 ) ) ;
#1685=VERTEX_POINT ( 'NONE', #4658 ) ;
#1705=LINE ( 'NONE', #16054, #16773 ) ;
#1723=CYLINDRICAL_SURFACE ( 'NONE', #13950, 25.25038683781155413 ) ;
#1809=LINE ( 'NONE', #12367, #4985 ) ;
#1843=( NAMED_UNIT ( * ) PLANE_ANGLE_UNIT ( ) SI_UNIT ( $, .RADIAN. ) );
#1866=VECTOR ( 'NONE', #11670, 1000.000000000000000 ) ;
#1901=ORIENTED_EDGE ( 'NONE', *, *, #14116, .T. ) ;
#1957=ADVANCED_FACE ( 'NONE', ( #9966 ), #1723, .F. ) ;
#1967=DIRECTION ( 'NONE',  ( -1.000000000000000000, 0.000000000000000000, -0.000000000000000000 ) ) ;
#1973=ADVANCED_BREP_SHAPE_REPRESENTATION ( '', ( #2742, #1488 ), #4776 ) ;
#2027=EDGE_LOOP ( 'NONE', ( #12817, #3120, #13749, #13996 ) ) ;
#2095=DIRECTION ( 'NONE',  ( -1.000000000000000000, -0.000000000000000000, -0.000000000000000000 ) ) ;
#2143=LINE ( 'NONE', #5846, #15483 ) ;
#2154=DIRECTION ( 'NONE',  ( -1.000000000000000000, -0.000000000000000000, -0.000000000000000000 ) ) ;
#2270=DIRECTION ( 'NONE',  ( 0.000000000000000000, 0.000000000000000000, -1.000000000000000000 ) ) ;
#2360=EDGE_CURVE ( 'NONE', #6025, #4071, #4172, .T. ) ;
#2375=DIRECTION ( 'NONE',  ( 1.000000000000000000, -0.000000000000000000, 0.000000000000000000 ) ) ;
#2456=ADVANCED_FACE ( 'NONE', ( #901 ), #7150, .F. ) ;
#2470=CARTESIAN_POINT ( 'NONE',  ( 0.000000000000000000, 481.5601199098531993, -512.1772732904406666 ) ) ;
#2473=CARTESIAN_POINT ( 'NONE',  ( 0.000000000000000000, 226.8713558223388134, -346.2582248962859808 ) ) ;
#2511=CARTESIAN_POINT ( 'NONE',  ( 0.000000000000000000, 364.9870314427752191, -206.3519347178565795 ) ) ;
#2519=AXIS2_PLACEMENT_3D ( 'NONE', #16622, #11464, #10357 ) ;
#2605=DIRECTION ( 'NONE',  ( 0.000000000000000000, 0.3853514969300962378, 0.9227698650333863162 ) ) ;
#2610=ORIENTED_EDGE ( 'NONE', *, *, #1301, .T. ) ;
#2630=DIRECTION ( 'NONE',  ( 0.000000000000000000, 0.000000000000000000, -1.000000000000000000 ) ) ;
#2638=ORIENTED_EDGE ( 'NONE', *, *, #4767, .F. ) ;
#2649=CARTESIAN_POINT ( 'NONE',  ( 10.00000000000000000, 34.88079231221936283, 28.80067286797032722 ) ) ;
#2658=EDGE_LOOP ( 'NONE', ( #682, #2638 ) ) ;
#2663=CYLINDRICAL_SURFACE ( 'NONE', #5586, 29.99999999999530687 ) ;
#2702=APPLICATION_CONTEXT ( 'automotive_design' ) ;
#2717=CARTESIAN_POINT ( 'NONE',  ( 0.000000000000000000, 435.2933666400819561, -550.3792044179907634 ) ) ;
#2724=AXIS2_PLACEMENT_3D ( 'NONE', #3453, #15118, #8606 ) ;
#2740=VERTEX_POINT ( 'NONE', #1662 ) ;
#2742=MANIFOLD_SOLID_BREP ( 'Cut-Extrude1', #9103 ) ;
#2888=CIRCLE ( 'NONE', #1245, 59.99999999999982947 ) ;
#2908=VERTEX_POINT ( 'NONE', #16917 ) ;
#2914=CARTESIAN_POINT ( 'NONE',  ( 10.00000000000000000, 336.2713855965630501, -311.0652884549417081 ) ) ;
#2917=CARTESIAN_POINT ( 'NONE',  ( 10.00000000000000000, 226.8713558223388134, -346.2582248962859808 ) ) ;
#2979=DIRECTION ( 'NONE',  ( -1.000000000000000000, 0.000000000000000000, -0.000000000000000000 ) ) ;
#3097=DIRECTION ( 'NONE',  ( -1.000000000000000000, -0.000000000000000000, -0.000000000000000000 ) ) ;
#3120=ORIENTED_EDGE ( 'NONE', *, *, #13473, .F. ) ;
#3201=DIRECTION ( 'NONE',  ( -1.000000000000000000, -0.000000000000000000, -0.000000000000000000 ) ) ;
#3280=CARTESIAN_POINT ( 'NONE',  ( 0.000000000000000000, 0.000000000000000000, 0.000000000000000000 ) ) ;
#3337=ORIENTED_EDGE ( 'NONE', *, *, #5744, .F. ) ;
#3348=VECTOR ( 'NONE', #2154, 1000.000000000000000 ) ;
#3402=ORIENTED_EDGE ( 'NONE', *, *, #4094, .F. ) ;
#3431=ORIENTED_EDGE ( 'NONE', *, *, #5653, .F. ) ;
#3453=CARTESIAN_POINT ( 'NONE',  ( 0.000000000000000000, 226.8713558223388134, -346.2582248962859808 ) ) ;
#3468=CIRCLE ( 'NONE', #13346, 59.99999999999982947 ) ;
#3482=CYLINDRICAL_SURFACE ( 'NONE', #11707, 25.25038683781155413 ) ;
#3484=DIRECTION ( 'NONE',  ( -1.000000000000000000, -0.000000000000000000, -0.000000000000000000 ) ) ;
#3536=DIRECTION ( 'NONE',  ( 0.000000000000000000, 0.000000000000000000, -1.000000000000000000 ) ) ;
#3555=CARTESIAN_POINT ( 'NONE',  ( 10.00000000000000000, 226.8713558223388134, -358.7582248962859808 ) ) ;
#3605=EDGE_CURVE ( 'NONE', #7059, #8520, #15741, .T. ) ;
#3656=AXIS2_PLACEMENT_3D ( 'NONE', #7999, #11619, #15737 ) ;
#3772=AXIS2_PLACEMENT_3D ( 'NONE', #2649, #12874, #1363 ) ;
#3809=LINE ( 'NONE', #11706, #9973 ) ;
#3872=DIRECTION ( 'NONE',  ( 0.000000000000000000, 0.000000000000000000, 1.000000000000000000 ) ) ;
#3897=CARTESIAN_POINT ( 'NONE',  ( 10.00000000000000000, 435.2933666400819561, -575.6295912558023247 ) ) ;
#3959=ORIENTED_EDGE ( 'NONE', *, *, #11735, .F. ) ;
#4033=CYLINDRICAL_SURFACE ( 'NONE', #9263, 12.50000000000001066 ) ;
#4071=VERTEX_POINT ( 'NONE', #6788 ) ;
#4094=EDGE_CURVE ( 'NONE', #2740, #15912, #9453, .T. ) ;
#4163=FACE_BOUND ( 'NONE', #7037, .T. ) ;
#4168=DIRECTION ( 'NONE',  ( -1.000000000000000000, -0.000000000000000000, -0.000000000000000000 ) ) ;
#4172=LINE ( 'NONE', #7075, #11210 ) ;
#4187=VECTOR ( 'NONE', #14049, 1000.000000000000000 ) ;
#4215=CYLINDRICAL_SURFACE ( 'NONE', #8669, 59.99999999999982947 ) ;
#4283=EDGE_CURVE ( 'NONE', #2908, #2740, #2143, .T. ) ;
#4307=UNCERTAINTY_MEASURE_WITH_UNIT (LENGTH_MEASURE( 1.000000000000000082E-05 ), #12057, 'distance_accuracy_value', 'NONE');
#4346=DIRECTION ( 'NONE',  ( 1.000000000000000000, -0.000000000000000000, 0.000000000000000000 ) ) ;
#4355=DIRECTION ( 'NONE',  ( 0.000000000000000000, 0.000000000000000000, -1.000000000000000000 ) ) ;
#4356=LINE ( 'NONE', #12078, #70 ) ;
#4400=DIRECTION ( 'NONE',  ( 0.000000000000000000, 0.000000000000000000, -1.000000000000000000 ) ) ;
#4430=CARTESIAN_POINT ( 'NONE',  ( 0.000000000000000000, 340.8211049126788907, -341.7267989266199493 ) ) ;
#4448=EDGE_LOOP ( 'NONE', ( #4504, #14702, #8506, #7747 ) ) ;
#4474=ORIENTED_EDGE ( 'NONE', *, *, #11704, .T. ) ;
#4498=VECTOR ( 'NONE', #2095, 1000.000000000000000 ) ;
#4504=ORIENTED_EDGE ( 'NONE', *, *, #8793, .T. ) ;
#4528=CIRCLE ( 'NONE', #14685, 25.25038683781155413 ) ;
#4537=ORIENTED_EDGE ( 'NONE', *, *, #3605, .T. ) ;
#4556=EDGE_CURVE ( 'NONE', #13387, #10318, #13595, .T. ) ;
#4564=FACE_OUTER_BOUND ( 'NONE', #1305, .T. ) ;
#4566=ORIENTED_EDGE ( 'NONE', *, *, #4767, .T. ) ;
#4600=FACE_OUTER_BOUND ( 'NONE', #5864, .T. ) ;
#4638=DIRECTION ( 'NONE',  ( 1.000000000000000000, 0.000000000000000000, 0.000000000000000000 ) ) ;
#4651=AXIS2_PLACEMENT_3D ( 'NONE', #9167, #2375, #2630 ) ;
#4658=CARTESIAN_POINT ( 'NONE',  ( 0.000000000000000000, 226.8713558223388134, -333.7582248962859808 ) ) ;
#4673=VERTEX_POINT ( 'NONE', #9792 ) ;
#4745=COLOUR_RGB ( '', 0.09019608, 0.27058824, 0.51372549) ;
#4750=CARTESIAN_POINT ( 'NONE',  ( 10.00000000000000000, 336.2713855965630501, -311.0652884549417081 ) ) ;
#4754=DIRECTION ( 'NONE',  ( 0.000000000000000000, 0.000000000000000000, 1.000000000000000000 ) ) ;
#4767=EDGE_CURVE ( 'NONE', #785, #2908, #4528, .T. ) ;
#4776=( GEOMETRIC_REPRESENTATION_CONTEXT ( 3 ) GLOBAL_UNCERTAINTY_ASSIGNED_CONTEXT ( ( #15799 ) ) GLOBAL_UNIT_ASSIGNED_CONTEXT ( ( #391, #1843, #12565 ) ) REPRESENTATION_CONTEXT ( 'NONE', 'WORKASPACE' ) );
#4781=APPLICATION_CONTEXT ( 'automotive_design' ) ;
#4787=ORIENTED_EDGE ( 'NONE', *, *, #5809, .F. ) ;
#4837=PRODUCT_DEFINITION ( 'UNKNOWN', '', #1218, #7422 ) ;
#4840=FACE_OUTER_BOUND ( 'NONE', #2027, .T. ) ;
#4914=CARTESIAN_POINT ( 'NONE',  ( 10.00000000000000000, 202.9739201934855828, -514.2167050642598269 ) ) ;
#4985=VECTOR ( 'NONE', #15104, 1000.000000000000000 ) ;
#4989=VECTOR ( 'NONE', #13376, 1000.000000000000000 ) ;
#5017=CARTESIAN_POINT ( 'NONE',  ( 0.000000000000000000, 226.8713558223388134, -346.2582248962859808 ) ) ;
#5032=EDGE_CURVE ( 'NONE', #7243, #12507, #2888, .T. ) ;
#5039=VERTEX_POINT ( 'NONE', #13121 ) ;
#5100=DIRECTION ( 'NONE',  ( -1.000000000000000000, 0.000000000000000000, -0.000000000000000000 ) ) ;
#5125=LINE ( 'NONE', #7613, #84 ) ;
#5147=CARTESIAN_POINT ( 'NONE',  ( 10.00000000000000000, 185.0000000000000000, -486.7326477857670852 ) ) ;
#5226=DIRECTION ( 'NONE',  ( -1.000000000000000000, -0.000000000000000000, -0.000000000000000000 ) ) ;
#5231=ORIENTED_EDGE ( 'NONE', *, *, #498, .F. ) ;
#5240=CIRCLE ( 'NONE', #14869, 12.50000000000001066 ) ;
#5273=CARTESIAN_POINT ( 'NONE',  ( 0.000000000000000000, 364.9870314427736275, -216.3519347178565795 ) ) ;
#5305=FACE_OUTER_BOUND ( 'NONE', #16675, .T. ) ;
#5340=ORIENTED_EDGE ( 'NONE', *, *, #8399, .F. ) ;
#5361=FACE_OUTER_BOUND ( 'NONE', #1262, .T. ) ;
#5425=VERTEX_POINT ( 'NONE', #14734 ) ;
#5473=DIRECTION ( 'NONE',  ( 0.000000000000000000, -9.899245676326632924E-17, -1.000000000000000000 ) ) ;
#5517=AXIS2_PLACEMENT_3D ( 'NONE', #310, #8199, #10950 ) ;
#5532=CIRCLE ( 'NONE', #7711, 12.50000000000001066 ) ;
#5535=VECTOR ( 'NONE', #4168, 1000.000000000000000 ) ;
#5552=CARTESIAN_POINT ( 'NONE',  ( 10.00000000000000000, 481.5601199098531993, -512.1772732904406666 ) ) ;
#5563=ORIENTED_EDGE ( 'NONE', *, *, #4094, .T. ) ;
#5581=ORIENTED_EDGE ( 'NONE', *, *, #5809, .T. ) ;
#5586=AXIS2_PLACEMENT_3D ( 'NONE', #11768, #5226, #3872 ) ;
#5620=FACE_BOUND ( 'NONE', #9829, .T. ) ;
#5653=EDGE_CURVE ( 'NONE', #7243, #13274, #14602, .T. ) ;
#5694=PRESENTATION_STYLE_ASSIGNMENT (( #10939 ) ) ;
#5717=ADVANCED_FACE ( 'NONE', ( #1465 ), #4215, .T. ) ;
#5739=ORIENTED_EDGE ( 'NONE', *, *, #10666, .T. ) ;
#5744=EDGE_CURVE ( 'NONE', #5425, #11, #3468, .T. ) ;
#5809=EDGE_CURVE ( 'NONE', #15912, #2740, #13070, .T. ) ;
#5833=CARTESIAN_POINT ( 'NONE',  ( 10.00000000000000000, 226.8713558223388134, -346.2582248962859808 ) ) ;
#5846=CARTESIAN_POINT ( 'NONE',  ( 10.00000000000000000, 435.2933666400819561, -525.1288175801793159 ) ) ;
#5864=EDGE_LOOP ( 'NONE', ( #11608, #14471, #5868, #6315 ) ) ;
#5868=ORIENTED_EDGE ( 'NONE', *, *, #66, .F. ) ;
#5883=FACE_OUTER_BOUND ( 'NONE', #16005, .T. ) ;
#5902=ORIENTED_EDGE ( 'NONE', *, *, #13843, .F. ) ;
#5919=DIRECTION ( 'NONE',  ( 1.000000000000000000, -0.000000000000000000, 0.000000000000000000 ) ) ;
#5921=DIRECTION ( 'NONE',  ( 0.000000000000000000, 0.000000000000000000, -1.000000000000000000 ) ) ;
#5926=AXIS2_PLACEMENT_3D ( 'NONE', #13741, #5919, #16565 ) ;
#5961=CARTESIAN_POINT ( 'NONE',  ( 10.00000000000000000, 396.9484440344699010, -165.7668752622531088 ) ) ;
#6025=VERTEX_POINT ( 'NONE', #10806 ) ;
#6074=DIRECTION ( 'NONE',  ( 0.000000000000000000, -1.850371707708599493E-15, -1.000000000000000000 ) ) ;
#6078=CARTESIAN_POINT ( 'NONE',  ( 0.000000000000000000, 226.8713558223388134, -358.7582248962859808 ) ) ;
#6108=ORIENTED_EDGE ( 'NONE', *, *, #2360, .F. ) ;
#6109=VECTOR ( 'NONE', #2605, 1000.000000000000114 ) ;
#6122=CARTESIAN_POINT ( 'NONE',  ( 10.00000000000000000, 185.0000000000000568, -1.831360450120427585E-14 ) ) ;
#6222=ORIENTED_EDGE ( 'NONE', *, *, #2360, .T. ) ;
#6278=CARTESIAN_POINT ( 'NONE',  ( 10.00000000000000000, 226.8713558223388134, -333.7582248962859808 ) ) ;
#6315=ORIENTED_EDGE ( 'NONE', *, *, #13473, .T. ) ;
#6397=VECTOR ( 'NONE', #13047, 1000.000000000000114 ) ;
#6412=LINE ( 'NONE', #6680, #1866 ) ;
#6492=CARTESIAN_POINT ( 'NONE',  ( 0.000000000000000000, 411.2412070270587492, -605.3473189749742005 ) ) ;
#6514=DIRECTION ( 'NONE',  ( -1.000000000000000000, -0.000000000000000000, -0.000000000000000000 ) ) ;
#6547=ORIENTED_EDGE ( 'NONE', *, *, #10665, .F. ) ;
#6587=FACE_BOUND ( 'NONE', #2658, .T. ) ;
#6637=AXIS2_PLACEMENT_3D ( 'NONE', #6122, #11124, #9919 ) ;
#6680=CARTESIAN_POINT ( 'NONE',  ( 10.00000000000000000, 411.2412070270587492, -605.3473189749742005 ) ) ;
#6694=ORIENTED_EDGE ( 'NONE', *, *, #14147, .T. ) ;
#6723=VERTEX_POINT ( 'NONE', #9821 ) ;
#6788=CARTESIAN_POINT ( 'NONE',  ( 10.00000000000000000, 185.0000000000000284, -206.3519347178565795 ) ) ;
#6811=EDGE_CURVE ( 'NONE', #13919, #5039, #1296, .T. ) ;
#6893=ORIENTED_EDGE ( 'NONE', *, *, #1420, .T. ) ;
#6896=CARTESIAN_POINT ( 'NONE',  ( 0.000000000000000000, 0.000000000000000000, 0.000000000000000000 ) ) ;
#6983=ORIENTED_EDGE ( 'NONE', *, *, #12460, .F. ) ;
#6996=DIRECTION ( 'NONE',  ( 0.000000000000000000, -1.000000000000000000, 0.000000000000000000 ) ) ;
#7037=EDGE_LOOP ( 'NONE', ( #1901, #5739 ) ) ;
#7040=VERTEX_POINT ( 'NONE', #6078 ) ;
#7059=VERTEX_POINT ( 'NONE', #14080 ) ;
#7073=LINE ( 'NONE', #4750, #4498 ) ;
#7075=CARTESIAN_POINT ( 'NONE',  ( 10.00000000000000000, 0.000000000000000000, -206.3519347178565795 ) ) ;
#7103=DIRECTION ( 'NONE',  ( 1.000000000000000000, -0.000000000000000000, 0.000000000000000000 ) ) ;
#7150=PLANE ( 'NONE',  #6637 ) ;
#7230=AXIS2_PLACEMENT_3D ( 'NONE', #5833, #11081, #5921 ) ;
#7243=VERTEX_POINT ( 'NONE', #2470 ) ;
#7327=PLANE ( 'NONE',  #643 ) ;
#7422=PRODUCT_DEFINITION_CONTEXT ( 'detailed design', #2702, 'design' ) ;
#7610=EDGE_CURVE ( 'NONE', #10013, #7981, #1279, .T. ) ;
#7613=CARTESIAN_POINT ( 'NONE',  ( 0.000000000000000000, 185.0000000000000568, -1.831360450120427585E-14 ) ) ;
#7624=PLANE ( 'NONE',  #3772 ) ;
#7650=DIRECTION ( 'NONE',  ( -1.000000000000000000, -0.000000000000000000, -0.000000000000000000 ) ) ;
#7711=AXIS2_PLACEMENT_3D ( 'NONE', #12631, #4638, #3536 ) ;
#7747=ORIENTED_EDGE ( 'NONE', *, *, #6811, .T. ) ;
#7787=CARTESIAN_POINT ( 'NONE',  ( 0.000000000000000000, -156.2292101480469739, -357.0417483806770633 ) ) ;
#7798=ADVANCED_FACE ( 'NONE', ( #5883 ), #3482, .F. ) ;
#7803=DIRECTION ( 'NONE',  ( 0.000000000000000000, 0.000000000000000000, -1.000000000000000000 ) ) ;
#7842=DIRECTION ( 'NONE',  ( -1.000000000000000000, -0.000000000000000000, -0.000000000000000000 ) ) ;
#7870=EDGE_LOOP ( 'NONE', ( #11558, #8074, #13179, #10675 ) ) ;
#7913=DIRECTION ( 'NONE',  ( 0.000000000000000000, 0.9161352426163912321, -0.4008693268837190127 ) ) ;
#7925=EDGE_CURVE ( 'NONE', #1685, #13387, #12662, .T. ) ;
#7932=DIRECTION ( 'NONE',  ( -0.000000000000000000, 0.4008693268837190127, 0.9161352426163912321 ) ) ;
#7981=VERTEX_POINT ( 'NONE', #2511 ) ;
#7999=CARTESIAN_POINT ( 'NONE',  ( 10.00000000000000000, 435.2933666400819561, -550.3792044179907634 ) ) ;
#8024=CARTESIAN_POINT ( 'NONE',  ( 10.00000000000000000, 435.2933666400819561, -575.6295912558023247 ) ) ;
#8074=ORIENTED_EDGE ( 'NONE', *, *, #14982, .F. ) ;
#8186=SURFACE_STYLE_FILL_AREA ( #9655 ) ;
#8199=DIRECTION ( 'NONE',  ( -1.000000000000000000, 0.000000000000000000, -0.000000000000000000 ) ) ;
#8353=AXIS2_PLACEMENT_3D ( 'NONE', #16793, #16634, #11311 ) ;
#8378=ADVANCED_FACE ( 'NONE', ( #15545 ), #4033, .F. ) ;
#8399=EDGE_CURVE ( 'NONE', #11, #12507, #6412, .T. ) ;
#8411=DIRECTION ( 'NONE',  ( 0.000000000000000000, 0.000000000000000000, -1.000000000000000000 ) ) ;
#8440=ADVANCED_FACE ( 'NONE', ( #5305 ), #7624, .F. ) ;
#8441=LINE ( 'NONE', #10069, #3348 ) ;
#8506=ORIENTED_EDGE ( 'NONE', *, *, #14147, .F. ) ;
#8520=VERTEX_POINT ( 'NONE', #2914 ) ;
#8524=ORIENTED_EDGE ( 'NONE', *, *, #10123, .F. ) ;
#8606=DIRECTION ( 'NONE',  ( 0.000000000000000000, 0.000000000000000000, -1.000000000000000000 ) ) ;
#8669=AXIS2_PLACEMENT_3D ( 'NONE', #1635, #3097, #351 ) ;
#8693=DIRECTION ( 'NONE',  ( 0.000000000000000000, 0.000000000000000000, 1.000000000000000000 ) ) ;
#8727=DIRECTION ( 'NONE',  ( 0.000000000000000000, 0.000000000000000000, 1.000000000000000000 ) ) ;
#8786=ORIENTED_EDGE ( 'NONE', *, *, #506, .F. ) ;
#8793=EDGE_CURVE ( 'NONE', #5039, #6723, #9603, .T. ) ;
#8825=ORIENTED_EDGE ( 'NONE', *, *, #14116, .F. ) ;
#8844=AXIS2_PLACEMENT_3D ( 'NONE', #13139, #9276, #7803 ) ;
#8868=MECHANICAL_DESIGN_GEOMETRIC_PRESENTATION_REPRESENTATION('',(#14342),#12718);
#8916=AXIS2_PLACEMENT_3D ( 'NONE', #2917, #10818, #13406 ) ;
#8964=EDGE_CURVE ( 'NONE', #8520, #15272, #11044, .T. ) ;
#9004=CARTESIAN_POINT ( 'NONE',  ( 0.000000000000000000, 226.8713558223388134, -358.7582248962859808 ) ) ;
#9070=ADVANCED_FACE ( 'NONE', ( #4600 ), #15251, .T. ) ;
#9103=CLOSED_SHELL ( 'NONE', ( #8378, #1957, #8440, #9200, #16821, #9070, #9133, #2456, #12098, #14185, #7798, #5717, #14458, #14179, #13423 ) ) ;
#9104=VECTOR ( 'NONE', #16799, 1000.000000000000000 ) ;
#9113=FACE_OUTER_BOUND ( 'NONE', #4448, .T. ) ;
#9130=ORIENTED_EDGE ( 'NONE', *, *, #5032, .T. ) ;
#9133=ADVANCED_FACE ( 'NONE', ( #1068 ), #15332, .F. ) ;
#9167=CARTESIAN_POINT ( 'NONE',  ( 0.000000000000000000, 214.9999999999953104, -486.7326477857724853 ) ) ;
#9200=ADVANCED_FACE ( 'NONE', ( #38 ), #16692, .F. ) ;
#9263=AXIS2_PLACEMENT_3D ( 'NONE', #2473, #12958, #13219 ) ;
#9276=DIRECTION ( 'NONE',  ( 1.000000000000000000, -0.000000000000000000, 0.000000000000000000 ) ) ;
#9280=DIRECTION ( 'NONE',  ( 0.000000000000000000, -0.6366988521258363232, 0.7711125544961918710 ) ) ;
#9406=ORIENTED_EDGE ( 'NONE', *, *, #7925, .T. ) ;
#9453=CIRCLE ( 'NONE', #16037, 25.25038683781155413 ) ;
#9498=PLANE ( 'NONE',  #11854 ) ;
#9523=DIRECTION ( 'NONE',  ( -1.000000000000000000, -0.000000000000000000, -0.000000000000000000 ) ) ;
#9579=CARTESIAN_POINT ( 'NONE',  ( 10.00000000000000000, -156.2292101480469739, -357.0417483806770633 ) ) ;
#9603=CIRCLE ( 'NONE', #4651, 29.99999999999530687 ) ;
#9625=PRODUCT ( 'Part5', 'Part5', '', ( #790 ) ) ;
#9655=FILL_AREA_STYLE ('',( #10594 ) ) ;
#9665=AXIS2_PLACEMENT_3D ( 'NONE', #15867, #12275, #8411 ) ;
#9726=ORIENTED_EDGE ( 'NONE', *, *, #1301, .F. ) ;
#9792=CARTESIAN_POINT ( 'NONE',  ( 10.00000000000000000, 202.9739201934855828, -514.2167050642598269 ) ) ;
#9800=CARTESIAN_POINT ( 'NONE',  ( 10.00000000000000000, 435.2933666400819561, -550.3792044179907634 ) ) ;
#9805=DIRECTION ( 'NONE',  ( 0.000000000000000000, 0.000000000000000000, 1.000000000000000000 ) ) ;
#9821=CARTESIAN_POINT ( 'NONE',  ( 0.000000000000000000, 202.9739201934855828, -514.2167050642598269 ) ) ;
#9829=EDGE_LOOP ( 'NONE', ( #5563, #5581 ) ) ;
#9849=CARTESIAN_POINT ( 'NONE',  ( 10.00000000000000000, 364.9870314427736275, -216.3519347178565795 ) ) ;
#9868=CARTESIAN_POINT ( 'NONE',  ( 10.00000000000000000, 435.2933666400819561, -550.3792044179907634 ) ) ;
#9919=DIRECTION ( 'NONE',  ( 0.000000000000000000, 9.899245676326632924E-17, 1.000000000000000000 ) ) ;
#9966=FACE_OUTER_BOUND ( 'NONE', #15442, .T. ) ;
#9972=ORIENTED_EDGE ( 'NONE', *, *, #7610, .F. ) ;
#9973=VECTOR ( 'NONE', #7913, 1000.000000000000114 ) ;
#10013=VERTEX_POINT ( 'NONE', #16857 ) ;
#10069=CARTESIAN_POINT ( 'NONE',  ( 10.00000000000000000, 185.0000000000000284, -206.3519347178565795 ) ) ;
#10076=ORIENTED_EDGE ( 'NONE', *, *, #4283, .F. ) ;
#10088=DIRECTION ( 'NONE',  ( 0.000000000000000000, -0.9227698650333863162, 0.3853514969300962378 ) ) ;
#10123=EDGE_CURVE ( 'NONE', #13274, #1501, #1405, .T. ) ;
#10191=ORIENTED_EDGE ( 'NONE', *, *, #498, .T. ) ;
#10217=CIRCLE ( 'NONE', #2519, 29.99999999999530687 ) ;
#10293=EDGE_LOOP ( 'NONE', ( #15135, #11745, #12149, #16611 ) ) ;
#10318=VERTEX_POINT ( 'NONE', #3555 ) ;
#10357=DIRECTION ( 'NONE',  ( 0.000000000000000000, 0.000000000000000000, -1.000000000000000000 ) ) ;
#10432=LINE ( 'NONE', #11638, #4187 ) ;
#10568=ORIENTED_EDGE ( 'NONE', *, *, #506, .T. ) ;
#10594=FILL_AREA_STYLE_COLOUR ( '', #4745 ) ;
#10605=ORIENTED_EDGE ( 'NONE', *, *, #66, .T. ) ;
#10665=EDGE_CURVE ( 'NONE', #4071, #15905, #8441, .T. ) ;
#10666=EDGE_CURVE ( 'NONE', #1685, #7040, #5532, .T. ) ;
#10675=ORIENTED_EDGE ( 'NONE', *, *, #8399, .T. ) ;
#10806=CARTESIAN_POINT ( 'NONE',  ( 10.00000000000000000, 364.9870314427752191, -206.3519347178565795 ) ) ;
#10818=DIRECTION ( 'NONE',  ( 1.000000000000000000, 0.000000000000000000, 0.000000000000000000 ) ) ;
#10939=SURFACE_STYLE_USAGE ( .BOTH. , #126 ) ;
#10950=DIRECTION ( 'NONE',  ( 0.000000000000000000, 0.000000000000000000, -1.000000000000000000 ) ) ;
#10988=EDGE_CURVE ( 'NONE', #7059, #13274, #1809, .T. ) ;
#11005=DIRECTION ( 'NONE',  ( -1.000000000000000000, -0.000000000000000000, -0.000000000000000000 ) ) ;
#11044=LINE ( 'NONE', #12416, #15625 ) ;
#11081=DIRECTION ( 'NONE',  ( 1.000000000000000000, 0.000000000000000000, 0.000000000000000000 ) ) ;
#11124=DIRECTION ( 'NONE',  ( 0.000000000000000000, 1.000000000000000000, -9.899245676326632924E-17 ) ) ;
#11166=LINE ( 'NONE', #7787, #6397 ) ;
#11210=VECTOR ( 'NONE', #6996, 1000.000000000000000 ) ;
#11311=DIRECTION ( 'NONE',  ( 0.000000000000000000, 0.000000000000000000, -1.000000000000000000 ) ) ;
#11335=CIRCLE ( 'NONE', #3656, 25.25038683781155413 ) ;
#11366=LINE ( 'NONE', #4914, #12722 ) ;
#11409=VECTOR ( 'NONE', #9280, 1000.000000000000000 ) ;
#11464=DIRECTION ( 'NONE',  ( 1.000000000000000000, -0.000000000000000000, 0.000000000000000000 ) ) ;
#11535=CARTESIAN_POINT ( 'NONE',  ( 0.000000000000000000, 226.8713558223388134, -333.7582248962859808 ) ) ;
#11558=ORIENTED_EDGE ( 'NONE', *, *, #5032, .F. ) ;
#11608=ORIENTED_EDGE ( 'NONE', *, *, #7610, .T. ) ;
#11619=DIRECTION ( 'NONE',  ( 1.000000000000000000, -0.000000000000000000, 0.000000000000000000 ) ) ;
#11638=CARTESIAN_POINT ( 'NONE',  ( 10.00000000000000000, 364.9870314427752191, -206.3519347178565795 ) ) ;
#11656=EDGE_CURVE ( 'NONE', #2908, #785, #11335, .T. ) ;
#11668=CARTESIAN_POINT ( 'NONE',  ( 10.00000000000000000, 411.2412070270587492, -605.3473189749742005 ) ) ;
#11670=DIRECTION ( 'NONE',  ( -1.000000000000000000, -0.000000000000000000, -0.000000000000000000 ) ) ;
#11704=EDGE_CURVE ( 'NONE', #4673, #11, #3809, .T. ) ;
#11706=CARTESIAN_POINT ( 'NONE',  ( 10.00000000000000000, -156.2292101480469739, -357.0417483806770633 ) ) ;
#11707=AXIS2_PLACEMENT_3D ( 'NONE', #14999, #15154, #4754 ) ;
#11712=DIRECTION ( 'NONE',  ( 1.000000000000000000, -0.000000000000000000, -0.000000000000000000 ) ) ;
#11735=EDGE_CURVE ( 'NONE', #1501, #10013, #1235, .T. ) ;
#11740=ORIENTED_EDGE ( 'NONE', *, *, #8964, .T. ) ;
#11745=ORIENTED_EDGE ( 'NONE', *, *, #16780, .F. ) ;
#11768=CARTESIAN_POINT ( 'NONE',  ( 10.00000000000000000, 214.9999999999953104, -486.7326477857724853 ) ) ;
#11854=AXIS2_PLACEMENT_3D ( 'NONE', #6896, #4346, #15754 ) ;
#12057=( LENGTH_UNIT ( ) NAMED_UNIT ( * ) SI_UNIT ( .MILLI., .METRE. ) );
#12078=CARTESIAN_POINT ( 'NONE',  ( 0.000000000000000000, -0.000000000000000000, -206.3519347178565795 ) ) ;
#12098=ADVANCED_FACE ( 'NONE', ( #9113 ), #2663, .T. ) ;
#12149=ORIENTED_EDGE ( 'NONE', *, *, #3605, .F. ) ;
#12216=DIRECTION ( 'NONE',  ( 1.000000000000000000, -0.000000000000000000, 0.000000000000000000 ) ) ;
#12225=EDGE_LOOP ( 'NONE', ( #10568, #6547, #6108, #12516 ) ) ;
#12264=AXIS2_PLACEMENT_3D ( 'NONE', #5273, #233, #4355 ) ;
#12268=LINE ( 'NONE', #5552, #12706 ) ;
#12275=DIRECTION ( 'NONE',  ( 1.000000000000000000, -0.000000000000000000, 0.000000000000000000 ) ) ;
#12297=CARTESIAN_POINT ( 'NONE',  ( 0.000000000000000000, 435.2933666400819561, -550.3792044179907634 ) ) ;
#12301=LINE ( 'NONE', #16333, #278 ) ;
#12367=CARTESIAN_POINT ( 'NONE',  ( 10.00000000000000000, 340.8211049126788907, -341.7267989266199493 ) ) ;
#12416=CARTESIAN_POINT ( 'NONE',  ( 10.00000000000000000, 396.9484440344699010, -165.7668752622531088 ) ) ;
#12460=EDGE_CURVE ( 'NONE', #10318, #13387, #15468, .T. ) ;
#12461=EDGE_CURVE ( 'NONE', #6723, #12507, #11166, .T. ) ;
#12507=VERTEX_POINT ( 'NONE', #6492 ) ;
#12516=ORIENTED_EDGE ( 'NONE', *, *, #14126, .T. ) ;
#12555=CARTESIAN_POINT ( 'NONE',  ( 0.000000000000000000, 185.0000000000000284, -206.3519347178565795 ) ) ;
#12565=( NAMED_UNIT ( * ) SI_UNIT ( $, .STERADIAN. ) SOLID_ANGLE_UNIT ( ) );
#12591=PRODUCT_DEFINITION_SHAPE ( 'NONE', 'NONE',  #4837 ) ;
#12631=CARTESIAN_POINT ( 'NONE',  ( 0.000000000000000000, 226.8713558223388134, -346.2582248962859808 ) ) ;
#12651=FACE_BOUND ( 'NONE', #12812, .T. ) ;
#12662=LINE ( 'NONE', #11535, #12806 ) ;
#12706=VECTOR ( 'NONE', #9523, 1000.000000000000000 ) ;
#12718=( GEOMETRIC_REPRESENTATION_CONTEXT ( 3 ) GLOBAL_UNCERTAINTY_ASSIGNED_CONTEXT ( ( #4307 ) ) GLOBAL_UNIT_ASSIGNED_CONTEXT ( ( #12057, #16169, #16087 ) ) REPRESENTATION_CONTEXT ( 'NONE', 'WORKASPACE' ) );
#12722=VECTOR ( 'NONE', #7650, 1000.000000000000000 ) ;
#12806=VECTOR ( 'NONE', #11712, 1000.000000000000000 ) ;
#12812=EDGE_LOOP ( 'NONE', ( #6983, #14637 ) ) ;
#12817=ORIENTED_EDGE ( 'NONE', *, *, #11735, .T. ) ;
#12874=DIRECTION ( 'NONE',  ( 0.000000000000000000, -0.7711125544961918710, -0.6366988521258363232 ) ) ;
#12920=DIRECTION ( 'NONE',  ( 0.000000000000000000, 0.000000000000000000, -1.000000000000000000 ) ) ;
#12958=DIRECTION ( 'NONE',  ( 1.000000000000000000, -0.000000000000000000, -0.000000000000000000 ) ) ;
#13024=CARTESIAN_POINT ( 'NONE',  ( 0.000000000000000000, 336.2713855965630501, -311.0652884549417081 ) ) ;
#13039=CARTESIAN_POINT ( 'NONE',  ( 10.00000000000000000, 185.0000000000000000, -486.7326477857670852 ) ) ;
#13047=DIRECTION ( 'NONE',  ( 0.000000000000000000, 0.9161352426163912321, -0.4008693268837190127 ) ) ;
#13069=ORIENTED_EDGE ( 'NONE', *, *, #11704, .F. ) ;
#13070=CIRCLE ( 'NONE', #5926, 25.25038683781155413 ) ;
#13097=DIRECTION ( 'NONE',  ( 0.000000000000000000, 0.000000000000000000, 1.000000000000000000 ) ) ;
#13121=CARTESIAN_POINT ( 'NONE',  ( 0.000000000000000000, 185.0000000000000000, -486.7326477857670852 ) ) ;
#13139=CARTESIAN_POINT ( 'NONE',  ( 10.00000000000000000, 0.000000000000000000, 0.000000000000000000 ) ) ;
#13179=ORIENTED_EDGE ( 'NONE', *, *, #5744, .T. ) ;
#13183=AXIS2_PLACEMENT_3D ( 'NONE', #14383, #7842, #13097 ) ;
#13219=DIRECTION ( 'NONE',  ( 0.000000000000000000, 0.000000000000000000, -1.000000000000000000 ) ) ;
#13274=VERTEX_POINT ( 'NONE', #4430 ) ;
#13279=DIRECTION ( 'NONE',  ( 0.000000000000000000, -0.9161352426163912321, 0.4008693268837190127 ) ) ;
#13296=ORIENTED_EDGE ( 'NONE', *, *, #7925, .F. ) ;
#13346=AXIS2_PLACEMENT_3D ( 'NONE', #9800, #1967, #6074 ) ;
#13376=DIRECTION ( 'NONE',  ( 0.000000000000000000, -0.6366988521258363232, 0.7711125544961918710 ) ) ;
#13387=VERTEX_POINT ( 'NONE', #6278 ) ;
#13406=DIRECTION ( 'NONE',  ( 0.000000000000000000, 0.000000000000000000, -1.000000000000000000 ) ) ;
#13415=CARTESIAN_POINT ( 'NONE',  ( 0.000000000000000000, 34.88079231221936283, 28.80067286797032722 ) ) ;
#13423=ADVANCED_FACE ( 'NONE', ( #4564 ), #15219, .F. ) ;
#13446=ORIENTED_EDGE ( 'NONE', *, *, #10665, .T. ) ;
#13473=EDGE_CURVE ( 'NONE', #15272, #10013, #12301, .T. ) ;
#13499=CIRCLE ( 'NONE', #9665, 10.00000000000061995 ) ;
#13586=CARTESIAN_POINT ( 'NONE',  ( 10.00000000000000000, 435.2933666400819561, -550.3792044179907634 ) ) ;
#13595=CIRCLE ( 'NONE', #8916, 12.50000000000001066 ) ;
#13679=ORIENTED_EDGE ( 'NONE', *, *, #12461, .T. ) ;
#13741=CARTESIAN_POINT ( 'NONE',  ( 0.000000000000000000, 435.2933666400819561, -550.3792044179907634 ) ) ;
#13749=ORIENTED_EDGE ( 'NONE', *, *, #8964, .F. ) ;
#13834=ORIENTED_EDGE ( 'NONE', *, *, #5653, .T. ) ;
#13843=EDGE_CURVE ( 'NONE', #7040, #10318, #14409, .T. ) ;
#13876=DIRECTION ( 'NONE',  ( 0.000000000000000000, 0.3853514969300962378, 0.9227698650333863162 ) ) ;
#13919=VERTEX_POINT ( 'NONE', #13039 ) ;
#13950=AXIS2_PLACEMENT_3D ( 'NONE', #13586, #609, #9805 ) ;
#13996=ORIENTED_EDGE ( 'NONE', *, *, #16780, .T. ) ;
#14049=DIRECTION ( 'NONE',  ( -1.000000000000000000, -0.000000000000000000, -0.000000000000000000 ) ) ;
#14080=CARTESIAN_POINT ( 'NONE',  ( 10.00000000000000000, 340.8211049126788907, -341.7267989266199493 ) ) ;
#14116=EDGE_CURVE ( 'NONE', #7040, #1685, #5240, .T. ) ;
#14126=EDGE_CURVE ( 'NONE', #6025, #7981, #10432, .T. ) ;
#14136=CARTESIAN_POINT ( 'NONE',  ( 10.00000000000000000, 0.000000000000000000, -206.3519347178565795 ) ) ;
#14147=EDGE_CURVE ( 'NONE', #13919, #4673, #10217, .T. ) ;
#14179=ADVANCED_FACE ( 'NONE', ( #4163, #5620, #5361 ), #9498, .F. ) ;
#14185=ADVANCED_FACE ( 'NONE', ( #138 ), #1593, .F. ) ;
#14342=STYLED_ITEM ( 'NONE', ( #5694 ), #2742 ) ;
#14372=CARTESIAN_POINT ( 'NONE',  ( 0.000000000000000000, 396.9484440344699010, -165.7668752622531088 ) ) ;
#14383=CARTESIAN_POINT ( 'NONE',  ( 10.00000000000000000, 363.9544815475646260, -322.6258333628447872 ) ) ;
#14407=DIRECTION ( 'NONE',  ( 0.000000000000000000, -1.850371707708599493E-15, -1.000000000000000000 ) ) ;
#14409=LINE ( 'NONE', #9004, #9104 ) ;
#14458=ADVANCED_FACE ( 'NONE', ( #12651, #6587, #91 ), #16904, .T. ) ;
#14471=ORIENTED_EDGE ( 'NONE', *, *, #14126, .F. ) ;
#14556=AXIS2_PLACEMENT_3D ( 'NONE', #14136, #2270, #5100 ) ;
#14559=EDGE_LOOP ( 'NONE', ( #13679, #5340, #13069, #137 ) ) ;
#14602=LINE ( 'NONE', #13415, #11409 ) ;
#14637=ORIENTED_EDGE ( 'NONE', *, *, #4556, .F. ) ;
#14685=AXIS2_PLACEMENT_3D ( 'NONE', #9868, #7103, #15098 ) ;
#14702=ORIENTED_EDGE ( 'NONE', *, *, #15607, .F. ) ;
#14734=CARTESIAN_POINT ( 'NONE',  ( 10.00000000000000000, 481.5601199098531993, -512.1772732904406666 ) ) ;
#14805=EDGE_CURVE ( 'NONE', #15905, #5039, #5125, .T. ) ;
#14817=AXIS2_PLACEMENT_3D ( 'NONE', #9849, #3484, #8727 ) ;
#14869=AXIS2_PLACEMENT_3D ( 'NONE', #5017, #911, #12920 ) ;
#14880=CARTESIAN_POINT ( 'NONE',  ( 0.000000000000000000, 435.2933666400819561, -575.6295912558023247 ) ) ;
#14982=EDGE_CURVE ( 'NONE', #5425, #7243, #12268, .T. ) ;
#14999=CARTESIAN_POINT ( 'NONE',  ( 10.00000000000000000, 435.2933666400819561, -550.3792044179907634 ) ) ;
#15098=DIRECTION ( 'NONE',  ( 0.000000000000000000, 0.000000000000000000, -1.000000000000000000 ) ) ;
#15104=DIRECTION ( 'NONE',  ( -1.000000000000000000, -0.000000000000000000, -0.000000000000000000 ) ) ;
#15118=DIRECTION ( 'NONE',  ( 1.000000000000000000, -0.000000000000000000, -0.000000000000000000 ) ) ;
#15135=ORIENTED_EDGE ( 'NONE', *, *, #10123, .T. ) ;
#15154=DIRECTION ( 'NONE',  ( -1.000000000000000000, -0.000000000000000000, -0.000000000000000000 ) ) ;
#15198=ORIENTED_EDGE ( 'NONE', *, *, #1420, .F. ) ;
#15217=DIRECTION ( 'NONE',  ( 1.000000000000000000, 0.000000000000000000, 0.000000000000000000 ) ) ;
#15219=CYLINDRICAL_SURFACE ( 'NONE', #2724, 12.50000000000001066 ) ;
#15251=CYLINDRICAL_SURFACE ( 'NONE', #14817, 10.00000000000061995 ) ;
#15272=VERTEX_POINT ( 'NONE', #1510 ) ;
#15332=PLANE ( 'NONE',  #14556 ) ;
#15442=EDGE_LOOP ( 'NONE', ( #16719, #6893, #3402, #10076 ) ) ;
#15468=CIRCLE ( 'NONE', #7230, 12.50000000000001066 ) ;
#15483=VECTOR ( 'NONE', #11005, 1000.000000000000000 ) ;
#15545=FACE_OUTER_BOUND ( 'NONE', #16423, .T. ) ;
#15553=VECTOR ( 'NONE', #6514, 1000.000000000000000 ) ;
#15607=EDGE_CURVE ( 'NONE', #4673, #6723, #11366, .T. ) ;
#15610=ORIENTED_EDGE ( 'NONE', *, *, #6811, .F. ) ;
#15625=VECTOR ( 'NONE', #13876, 1000.000000000000114 ) ;
#15689=DIRECTION ( 'NONE',  ( 0.000000000000000000, -9.899245676326632924E-17, -1.000000000000000000 ) ) ;
#15737=DIRECTION ( 'NONE',  ( 0.000000000000000000, 0.000000000000000000, -1.000000000000000000 ) ) ;
#15741=CIRCLE ( 'NONE', #8353, 30.00000000000002842 ) ;
#15754=DIRECTION ( 'NONE',  ( 0.000000000000000000, 0.000000000000000000, -1.000000000000000000 ) ) ;
#15799=UNCERTAINTY_MEASURE_WITH_UNIT (LENGTH_MEASURE( 1.000000000000000082E-05 ), #391, 'distance_accuracy_value', 'NONE');
#15867=CARTESIAN_POINT ( 'NONE',  ( 10.00000000000000000, 364.9870314427736275, -216.3519347178565795 ) ) ;
#15905=VERTEX_POINT ( 'NONE', #12555 ) ;
#15912=VERTEX_POINT ( 'NONE', #14880 ) ;
#15979=ORIENTED_EDGE ( 'NONE', *, *, #14982, .T. ) ;
#15980=ORIENTED_EDGE ( 'NONE', *, *, #4556, .T. ) ;
#16005=EDGE_LOOP ( 'NONE', ( #15198, #4566, #1563, #4787 ) ) ;
#16037=AXIS2_PLACEMENT_3D ( 'NONE', #12297, #12216, #4400 ) ;
#16054=CARTESIAN_POINT ( 'NONE',  ( 10.00000000000000000, 185.0000000000000568, -1.831360450120427585E-14 ) ) ;
#16087=( NAMED_UNIT ( * ) SI_UNIT ( $, .STERADIAN. ) SOLID_ANGLE_UNIT ( ) );
#16112=LINE ( 'NONE', #1601, #4989 ) ;
#16169=( NAMED_UNIT ( * ) PLANE_ANGLE_UNIT ( ) SI_UNIT ( $, .RADIAN. ) );
#16333=CARTESIAN_POINT ( 'NONE',  ( 10.00000000000000000, 374.2147300931088694, -220.2054496871573974 ) ) ;
#16348=SHAPE_REPRESENTATION_RELATIONSHIP ( 'NONE' , 'NONE' ,  #584, #1973 ) ;
#16351=ORIENTED_EDGE ( 'NONE', *, *, #12461, .F. ) ;
#16359=DIRECTION ( 'NONE',  ( 0.000000000000000000, -0.3853514969300962378, -0.9227698650333863162 ) ) ;
#16364=ORIENTED_EDGE ( 'NONE', *, *, #10988, .F. ) ;
#16423=EDGE_LOOP ( 'NONE', ( #724, #9406, #15980, #5902 ) ) ;
#16557=ORIENTED_EDGE ( 'NONE', *, *, #8793, .F. ) ;
#16565=DIRECTION ( 'NONE',  ( 0.000000000000000000, 0.000000000000000000, -1.000000000000000000 ) ) ;
#16611=ORIENTED_EDGE ( 'NONE', *, *, #10988, .T. ) ;
#16622=CARTESIAN_POINT ( 'NONE',  ( 10.00000000000000000, 214.9999999999953104, -486.7326477857724853 ) ) ;
#16634=DIRECTION ( 'NONE',  ( -1.000000000000000000, 0.000000000000000000, -0.000000000000000000 ) ) ;
#16675=EDGE_LOOP ( 'NONE', ( #13834, #16364, #5231, #15979 ) ) ;
#16692=CYLINDRICAL_SURFACE ( 'NONE', #13183, 30.00000000000002842 ) ;
#16719=ORIENTED_EDGE ( 'NONE', *, *, #11656, .T. ) ;
#16773=VECTOR ( 'NONE', #5473, 1000.000000000000000 ) ;
#16780=EDGE_CURVE ( 'NONE', #8520, #1501, #7073, .T. ) ;
#16793=CARTESIAN_POINT ( 'NONE',  ( 10.00000000000000000, 363.9544815475646260, -322.6258333628447872 ) ) ;
#16799=DIRECTION ( 'NONE',  ( 1.000000000000000000, -0.000000000000000000, -0.000000000000000000 ) ) ;
#16821=ADVANCED_FACE ( 'NONE', ( #4840 ), #7327, .F. ) ;
#16838=ORIENTED_EDGE ( 'NONE', *, *, #14805, .F. ) ;
#16857=CARTESIAN_POINT ( 'NONE',  ( 0.000000000000000000, 374.2147300931088694, -220.2054496871573974 ) ) ;
#16904=PLANE ( 'NONE',  #8844 ) ;
#16917=CARTESIAN_POINT ( 'NONE',  ( 10.00000000000000000, 435.2933666400819561, -525.1288175801793159 ) ) ;
ENDSEC;
END-ISO-10303-21;
